ISO-10303-21;
HEADER;
/* Generated by software containing ST-Developer
 * from STEP Tools, Inc. (www.steptools.com) 
 */

FILE_DESCRIPTION(
/* description */ ('PAT-015'),
/* implementation_level */ '2;1');

FILE_NAME(
/* name */ 'Hex Nut - M8.step',
/* time_stamp */ '2026-10-29T16:03:43-07:00',
/* author */ (''),
/* organization */ (''),
/* preprocessor_version */ 'ST-DEVELOPER v20.2',
/* originating_system */ 'Autodesk Translation Framework v15.17.0.0',
/* authorisation */ '');

FILE_SCHEMA (('AUTOMOTIVE_DESIGN { 1 0 10303 214 3 1 1 }'));
ENDSEC;

DATA;
#10=MECHANICAL_DESIGN_GEOMETRIC_PRESENTATION_REPRESENTATION('',(#250),#10266);
#151=(
BOUNDED_CURVE()
B_SPLINE_CURVE(2,(#9947,#9948,#9949),.UNSPECIFIED.,.F.,.F.)
B_SPLINE_CURVE_WITH_KNOTS((3,3),(0.14973948338295,0.97160236658079),
 .UNSPECIFIED.)
CURVE()
GEOMETRIC_REPRESENTATION_ITEM()
RATIONAL_B_SPLINE_CURVE((1.07140024848292,1.23714644374248,1.07140024848292))
REPRESENTATION_ITEM('')
);
#152=(
BOUNDED_CURVE()
B_SPLINE_CURVE(2,(#9951,#9952,#9953),.UNSPECIFIED.,.F.,.F.)
B_SPLINE_CURVE_WITH_KNOTS((3,3),(0.14973948338295,0.971602366580789),
 .UNSPECIFIED.)
CURVE()
GEOMETRIC_REPRESENTATION_ITEM()
RATIONAL_B_SPLINE_CURVE((1.07140024848292,1.23714644374248,1.07140024848292))
REPRESENTATION_ITEM('')
);
#153=(
BOUNDED_CURVE()
B_SPLINE_CURVE(2,(#9958,#9959,#9960),.UNSPECIFIED.,.F.,.F.)
B_SPLINE_CURVE_WITH_KNOTS((3,3),(0.14973948338295,0.97160236658079),
 .UNSPECIFIED.)
CURVE()
GEOMETRIC_REPRESENTATION_ITEM()
RATIONAL_B_SPLINE_CURVE((1.07140024848292,1.23714644374248,1.07140024848292))
REPRESENTATION_ITEM('')
);
#154=(
BOUNDED_CURVE()
B_SPLINE_CURVE(2,(#9962,#9963,#9964),.UNSPECIFIED.,.F.,.F.)
B_SPLINE_CURVE_WITH_KNOTS((3,3),(0.14973948338295,0.97160236658079),
 .UNSPECIFIED.)
CURVE()
GEOMETRIC_REPRESENTATION_ITEM()
RATIONAL_B_SPLINE_CURVE((1.07140024848292,1.23714644374248,1.07140024848292))
REPRESENTATION_ITEM('')
);
#155=(
BOUNDED_CURVE()
B_SPLINE_CURVE(2,(#9966,#9967,#9968),.UNSPECIFIED.,.F.,.F.)
B_SPLINE_CURVE_WITH_KNOTS((3,3),(0.14973948338295,0.971602366580789),
 .UNSPECIFIED.)
CURVE()
GEOMETRIC_REPRESENTATION_ITEM()
RATIONAL_B_SPLINE_CURVE((1.07140024848292,1.23714644374248,1.07140024848292))
REPRESENTATION_ITEM('')
);
#156=(
BOUNDED_CURVE()
B_SPLINE_CURVE(2,(#9969,#9970,#9971),.UNSPECIFIED.,.F.,.F.)
B_SPLINE_CURVE_WITH_KNOTS((3,3),(0.14973948338295,0.97160236658079),
 .UNSPECIFIED.)
CURVE()
GEOMETRIC_REPRESENTATION_ITEM()
RATIONAL_B_SPLINE_CURVE((1.07140024848292,1.23714644374248,1.07140024848292))
REPRESENTATION_ITEM('')
);
#157=(
BOUNDED_CURVE()
B_SPLINE_CURVE(2,(#9978,#9979,#9980),.UNSPECIFIED.,.F.,.F.)
B_SPLINE_CURVE_WITH_KNOTS((3,3),(0.14973948338295,0.97160236658079),
 .UNSPECIFIED.)
CURVE()
GEOMETRIC_REPRESENTATION_ITEM()
RATIONAL_B_SPLINE_CURVE((1.07140024848292,1.23714644374248,1.07140024848292))
REPRESENTATION_ITEM('')
);
#158=(
BOUNDED_CURVE()
B_SPLINE_CURVE(2,(#9982,#9983,#9984),.UNSPECIFIED.,.F.,.F.)
B_SPLINE_CURVE_WITH_KNOTS((3,3),(0.14973948338295,0.97160236658079),
 .UNSPECIFIED.)
CURVE()
GEOMETRIC_REPRESENTATION_ITEM()
RATIONAL_B_SPLINE_CURVE((1.07140024848292,1.23714644374248,1.07140024848292))
REPRESENTATION_ITEM('')
);
#159=(
BOUNDED_CURVE()
B_SPLINE_CURVE(2,(#9986,#9987,#9988),.UNSPECIFIED.,.F.,.F.)
B_SPLINE_CURVE_WITH_KNOTS((3,3),(0.14973948338295,0.971602366580789),
 .UNSPECIFIED.)
CURVE()
GEOMETRIC_REPRESENTATION_ITEM()
RATIONAL_B_SPLINE_CURVE((1.07140024848292,1.23714644374248,1.07140024848292))
REPRESENTATION_ITEM('')
);
#160=(
BOUNDED_CURVE()
B_SPLINE_CURVE(2,(#9990,#9991,#9992),.UNSPECIFIED.,.F.,.F.)
B_SPLINE_CURVE_WITH_KNOTS((3,3),(0.14973948338295,0.97160236658079),
 .UNSPECIFIED.)
CURVE()
GEOMETRIC_REPRESENTATION_ITEM()
RATIONAL_B_SPLINE_CURVE((1.07140024848292,1.23714644374248,1.07140024848292))
REPRESENTATION_ITEM('')
);
#161=(
BOUNDED_CURVE()
B_SPLINE_CURVE(2,(#9994,#9995,#9996),.UNSPECIFIED.,.F.,.F.)
B_SPLINE_CURVE_WITH_KNOTS((3,3),(0.14973948338295,0.97160236658079),
 .UNSPECIFIED.)
CURVE()
GEOMETRIC_REPRESENTATION_ITEM()
RATIONAL_B_SPLINE_CURVE((1.07140024848292,1.23714644374248,1.07140024848292))
REPRESENTATION_ITEM('')
);
#162=(
BOUNDED_CURVE()
B_SPLINE_CURVE(2,(#9997,#9998,#9999),.UNSPECIFIED.,.F.,.F.)
B_SPLINE_CURVE_WITH_KNOTS((3,3),(0.14973948338295,0.971602366580789),
 .UNSPECIFIED.)
CURVE()
GEOMETRIC_REPRESENTATION_ITEM()
RATIONAL_B_SPLINE_CURVE((1.07140024848292,1.23714644374248,1.07140024848292))
REPRESENTATION_ITEM('')
);
#174=CONICAL_SURFACE('',#5449,0.734027674973257,1.0471975511966);
#175=CONICAL_SURFACE('',#5451,0.734027674973257,1.0471975511966);
#202=SHAPE_REPRESENTATION_RELATIONSHIP('SRR','None',#10373,#225);
#225=ADVANCED_BREP_SHAPE_REPRESENTATION('',(#274),#10261);
#250=STYLED_ITEM('',(#10554),#274);
#274=MANIFOLD_SOLID_BREP('Body1',#4710);
#414=FACE_BOUND('',#1221,.T.);
#415=FACE_BOUND('',#1223,.T.);
#537=PLANE('',#5453);
#538=PLANE('',#5454);
#539=PLANE('',#5455);
#540=PLANE('',#5459);
#541=PLANE('',#5460);
#542=PLANE('',#5461);
#543=PLANE('',#5462);
#544=PLANE('',#5463);
#806=FACE_OUTER_BOUND('',#1211,.T.);
#807=FACE_OUTER_BOUND('',#1212,.T.);
#808=FACE_OUTER_BOUND('',#1213,.T.);
#809=FACE_OUTER_BOUND('',#1214,.T.);
#810=FACE_OUTER_BOUND('',#1215,.T.);
#811=FACE_OUTER_BOUND('',#1216,.T.);
#812=FACE_OUTER_BOUND('',#1217,.T.);
#813=FACE_OUTER_BOUND('',#1218,.T.);
#814=FACE_OUTER_BOUND('',#1219,.T.);
#815=FACE_OUTER_BOUND('',#1220,.T.);
#816=FACE_OUTER_BOUND('',#1222,.T.);
#1211=EDGE_LOOP('',(#4093,#4094,#4095,#4096,#4097,#4098,#4099,#4100,#4101));
#1212=EDGE_LOOP('',(#4102,#4103,#4104,#4105,#4106,#4107,#4108,#4109,#4110));
#1213=EDGE_LOOP('',(#4111,#4112,#4113,#4114));
#1214=EDGE_LOOP('',(#4115,#4116,#4117,#4118));
#1215=EDGE_LOOP('',(#4119,#4120,#4121,#4122));
#1216=EDGE_LOOP('',(#4123,#4124,#4125,#4126));
#1217=EDGE_LOOP('',(#4127,#4128,#4129,#4130));
#1218=EDGE_LOOP('',(#4131,#4132,#4133,#4134));
#1219=EDGE_LOOP('',(#4135,#4136,#4137,#4138));
#1220=EDGE_LOOP('',(#4139));
#1221=EDGE_LOOP('',(#4140));
#1222=EDGE_LOOP('',(#4141));
#1223=EDGE_LOOP('',(#4142));
#1536=LINE('',#9955,#1816);
#1537=LINE('',#9976,#1817);
#1538=LINE('',#10001,#1818);
#1539=LINE('',#10002,#1819);
#1540=LINE('',#10004,#1820);
#1541=LINE('',#10006,#1821);
#1542=LINE('',#10011,#1822);
#1543=LINE('',#10014,#1823);
#1544=LINE('',#10016,#1824);
#1816=VECTOR('',#6729,0.734027674973257);
#1817=VECTOR('',#6736,0.734027674973257);
#1818=VECTOR('',#6739,1.);
#1819=VECTOR('',#6740,1.);
#1820=VECTOR('',#6743,1.);
#1821=VECTOR('',#6746,1.);
#1822=VECTOR('',#6751,0.4);
#1823=VECTOR('',#6756,1.);
#1824=VECTOR('',#6759,1.);
#2094=CIRCLE('',#5450,0.6175);
#2095=CIRCLE('',#5452,0.6175);
#2096=CIRCLE('',#5457,0.338975);
#2097=CIRCLE('',#5458,0.338975);
#2443=VERTEX_POINT('',#9945);
#2444=VERTEX_POINT('',#9946);
#2445=VERTEX_POINT('',#9950);
#2446=VERTEX_POINT('',#9954);
#2447=VERTEX_POINT('',#9957);
#2448=VERTEX_POINT('',#9961);
#2449=VERTEX_POINT('',#9965);
#2450=VERTEX_POINT('',#9973);
#2451=VERTEX_POINT('',#9975);
#2452=VERTEX_POINT('',#9977);
#2453=VERTEX_POINT('',#9981);
#2454=VERTEX_POINT('',#9985);
#2455=VERTEX_POINT('',#9989);
#2456=VERTEX_POINT('',#9993);
#2457=VERTEX_POINT('',#10008);
#2458=VERTEX_POINT('',#10010);
#3002=EDGE_CURVE('',#2443,#2444,#151,.T.);
#3003=EDGE_CURVE('',#2445,#2443,#152,.T.);
#3004=EDGE_CURVE('',#2445,#2446,#1536,.T.);
#3005=EDGE_CURVE('',#2446,#2446,#2094,.T.);
#3006=EDGE_CURVE('',#2447,#2445,#153,.T.);
#3007=EDGE_CURVE('',#2448,#2447,#154,.T.);
#3008=EDGE_CURVE('',#2449,#2448,#155,.T.);
#3009=EDGE_CURVE('',#2444,#2449,#156,.T.);
#3010=EDGE_CURVE('',#2450,#2450,#2095,.T.);
#3011=EDGE_CURVE('',#2450,#2451,#1537,.T.);
#3012=EDGE_CURVE('',#2452,#2451,#157,.T.);
#3013=EDGE_CURVE('',#2453,#2452,#158,.T.);
#3014=EDGE_CURVE('',#2454,#2453,#159,.T.);
#3015=EDGE_CURVE('',#2455,#2454,#160,.T.);
#3016=EDGE_CURVE('',#2456,#2455,#161,.T.);
#3017=EDGE_CURVE('',#2451,#2456,#162,.T.);
#3018=EDGE_CURVE('',#2447,#2456,#1538,.T.);
#3019=EDGE_CURVE('',#2448,#2455,#1539,.T.);
#3020=EDGE_CURVE('',#2445,#2451,#1540,.T.);
#3021=EDGE_CURVE('',#2443,#2452,#1541,.T.);
#3022=EDGE_CURVE('',#2457,#2457,#2096,.F.);
#3023=EDGE_CURVE('',#2457,#2458,#1542,.T.);
#3024=EDGE_CURVE('',#2458,#2458,#2097,.F.);
#3025=EDGE_CURVE('',#2444,#2453,#1543,.T.);
#3026=EDGE_CURVE('',#2449,#2454,#1544,.T.);
#4093=ORIENTED_EDGE('',*,*,#3002,.F.);
#4094=ORIENTED_EDGE('',*,*,#3003,.F.);
#4095=ORIENTED_EDGE('',*,*,#3004,.T.);
#4096=ORIENTED_EDGE('',*,*,#3005,.F.);
#4097=ORIENTED_EDGE('',*,*,#3004,.F.);
#4098=ORIENTED_EDGE('',*,*,#3006,.F.);
#4099=ORIENTED_EDGE('',*,*,#3007,.F.);
#4100=ORIENTED_EDGE('',*,*,#3008,.F.);
#4101=ORIENTED_EDGE('',*,*,#3009,.F.);
#4102=ORIENTED_EDGE('',*,*,#3010,.F.);
#4103=ORIENTED_EDGE('',*,*,#3011,.T.);
#4104=ORIENTED_EDGE('',*,*,#3012,.F.);
#4105=ORIENTED_EDGE('',*,*,#3013,.F.);
#4106=ORIENTED_EDGE('',*,*,#3014,.F.);
#4107=ORIENTED_EDGE('',*,*,#3015,.F.);
#4108=ORIENTED_EDGE('',*,*,#3016,.F.);
#4109=ORIENTED_EDGE('',*,*,#3017,.F.);
#4110=ORIENTED_EDGE('',*,*,#3011,.F.);
#4111=ORIENTED_EDGE('',*,*,#3007,.T.);
#4112=ORIENTED_EDGE('',*,*,#3018,.T.);
#4113=ORIENTED_EDGE('',*,*,#3016,.T.);
#4114=ORIENTED_EDGE('',*,*,#3019,.F.);
#4115=ORIENTED_EDGE('',*,*,#3006,.T.);
#4116=ORIENTED_EDGE('',*,*,#3020,.T.);
#4117=ORIENTED_EDGE('',*,*,#3017,.T.);
#4118=ORIENTED_EDGE('',*,*,#3018,.F.);
#4119=ORIENTED_EDGE('',*,*,#3003,.T.);
#4120=ORIENTED_EDGE('',*,*,#3021,.T.);
#4121=ORIENTED_EDGE('',*,*,#3012,.T.);
#4122=ORIENTED_EDGE('',*,*,#3020,.F.);
#4123=ORIENTED_EDGE('',*,*,#3022,.F.);
#4124=ORIENTED_EDGE('',*,*,#3023,.T.);
#4125=ORIENTED_EDGE('',*,*,#3024,.T.);
#4126=ORIENTED_EDGE('',*,*,#3023,.F.);
#4127=ORIENTED_EDGE('',*,*,#3002,.T.);
#4128=ORIENTED_EDGE('',*,*,#3025,.T.);
#4129=ORIENTED_EDGE('',*,*,#3013,.T.);
#4130=ORIENTED_EDGE('',*,*,#3021,.F.);
#4131=ORIENTED_EDGE('',*,*,#3008,.T.);
#4132=ORIENTED_EDGE('',*,*,#3019,.T.);
#4133=ORIENTED_EDGE('',*,*,#3015,.T.);
#4134=ORIENTED_EDGE('',*,*,#3026,.F.);
#4135=ORIENTED_EDGE('',*,*,#3009,.T.);
#4136=ORIENTED_EDGE('',*,*,#3026,.T.);
#4137=ORIENTED_EDGE('',*,*,#3014,.T.);
#4138=ORIENTED_EDGE('',*,*,#3025,.F.);
#4139=ORIENTED_EDGE('',*,*,#3010,.T.);
#4140=ORIENTED_EDGE('',*,*,#3022,.T.);
#4141=ORIENTED_EDGE('',*,*,#3005,.T.);
#4142=ORIENTED_EDGE('',*,*,#3024,.F.);
#4401=CYLINDRICAL_SURFACE('',#5456,0.338975);
#4641=ADVANCED_FACE('',(#806),#174,.T.);
#4642=ADVANCED_FACE('',(#807),#175,.T.);
#4643=ADVANCED_FACE('',(#808),#537,.T.);
#4644=ADVANCED_FACE('',(#809),#538,.T.);
#4645=ADVANCED_FACE('',(#810),#539,.T.);
#4646=ADVANCED_FACE('',(#811),#4401,.F.);
#4647=ADVANCED_FACE('',(#812),#540,.T.);
#4648=ADVANCED_FACE('',(#813),#541,.T.);
#4649=ADVANCED_FACE('',(#814),#542,.T.);
#4650=ADVANCED_FACE('',(#815,#414),#543,.T.);
#4651=ADVANCED_FACE('',(#816,#415),#544,.F.);
#4710=CLOSED_SHELL('',(#4641,#4642,#4643,#4644,#4645,#4646,#4647,#4648,
#4649,#4650,#4651));
#5448=AXIS2_PLACEMENT_3D('',#9943,#6725,#6726);
#5449=AXIS2_PLACEMENT_3D('',#9944,#6727,#6728);
#5450=AXIS2_PLACEMENT_3D('',#9956,#6730,#6731);
#5451=AXIS2_PLACEMENT_3D('',#9972,#6732,#6733);
#5452=AXIS2_PLACEMENT_3D('',#9974,#6734,#6735);
#5453=AXIS2_PLACEMENT_3D('',#10000,#6737,#6738);
#5454=AXIS2_PLACEMENT_3D('',#10003,#6741,#6742);
#5455=AXIS2_PLACEMENT_3D('',#10005,#6744,#6745);
#5456=AXIS2_PLACEMENT_3D('',#10007,#6747,#6748);
#5457=AXIS2_PLACEMENT_3D('',#10009,#6749,#6750);
#5458=AXIS2_PLACEMENT_3D('',#10012,#6752,#6753);
#5459=AXIS2_PLACEMENT_3D('',#10013,#6754,#6755);
#5460=AXIS2_PLACEMENT_3D('',#10015,#6757,#6758);
#5461=AXIS2_PLACEMENT_3D('',#10017,#6760,#6761);
#5462=AXIS2_PLACEMENT_3D('',#10018,#6762,#6763);
#5463=AXIS2_PLACEMENT_3D('',#10019,#6764,#6765);
#6725=DIRECTION('axis',(0.,0.,1.));
#6726=DIRECTION('refdir',(1.,0.,0.));
#6727=DIRECTION('center_axis',(0.,1.,0.));
#6728=DIRECTION('ref_axis',(1.,0.,0.));
#6729=DIRECTION('',(0.866025403784439,-0.5,1.06057523872491E-16));
#6730=DIRECTION('center_axis',(0.,-1.,0.));
#6731=DIRECTION('ref_axis',(1.,0.,0.));
#6732=DIRECTION('center_axis',(0.,-1.,0.));
#6733=DIRECTION('ref_axis',(1.,0.,0.));
#6734=DIRECTION('center_axis',(0.,1.,0.));
#6735=DIRECTION('ref_axis',(1.,0.,0.));
#6736=DIRECTION('',(-0.866025403784439,-0.5,-1.06057523872491E-16));
#6737=DIRECTION('center_axis',(1.4792020664489E-16,0.,-1.));
#6738=DIRECTION('ref_axis',(-1.,0.,-1.4792020664489E-16));
#6739=DIRECTION('',(0.,1.,0.));
#6740=DIRECTION('',(0.,1.,0.));
#6741=DIRECTION('center_axis',(-0.866025403784439,0.,-0.5));
#6742=DIRECTION('ref_axis',(-0.5,0.,0.866025403784439));
#6743=DIRECTION('',(0.,1.,0.));
#6744=DIRECTION('center_axis',(-0.866025403784439,0.,0.5));
#6745=DIRECTION('ref_axis',(0.5,0.,0.866025403784439));
#6746=DIRECTION('',(0.,1.,0.));
#6747=DIRECTION('center_axis',(0.,1.,0.));
#6748=DIRECTION('ref_axis',(1.,0.,0.));
#6749=DIRECTION('center_axis',(0.,1.,0.));
#6750=DIRECTION('ref_axis',(1.,0.,0.));
#6751=DIRECTION('',(0.,-1.,0.));
#6752=DIRECTION('center_axis',(0.,1.,0.));
#6753=DIRECTION('ref_axis',(1.,0.,0.));
#6754=DIRECTION('center_axis',(-2.95840413289779E-16,0.,1.));
#6755=DIRECTION('ref_axis',(1.,0.,2.95840413289779E-16));
#6756=DIRECTION('',(0.,1.,0.));
#6757=DIRECTION('center_axis',(0.866025403784439,0.,-0.5));
#6758=DIRECTION('ref_axis',(-0.5,0.,-0.866025403784439));
#6759=DIRECTION('',(0.,1.,0.));
#6760=DIRECTION('center_axis',(0.866025403784439,0.,0.5));
#6761=DIRECTION('ref_axis',(0.5,0.,-0.866025403784439));
#6762=DIRECTION('center_axis',(0.,1.,0.));
#6763=DIRECTION('ref_axis',(1.,0.,0.));
#6764=DIRECTION('center_axis',(0.,1.,0.));
#6765=DIRECTION('ref_axis',(1.,0.,0.));
#9943=CARTESIAN_POINT('',(0.,0.,0.));
#9944=CARTESIAN_POINT('Origin',(0.,0.067277284513851,0.));
#9945=CARTESIAN_POINT('',(-0.375277674973257,0.0768195421087395,0.65));
#9946=CARTESIAN_POINT('',(0.375277674973257,0.0768195421087395,0.65));
#9947=CARTESIAN_POINT('Ctrl Pts',(-0.375277674973257,0.0768195421087395,
0.65));
#9948=CARTESIAN_POINT('Ctrl Pts',(1.66533453693773E-13,-0.0315137912242439,
0.65));
#9949=CARTESIAN_POINT('Ctrl Pts',(0.375277674973257,0.0768195421087394,
0.65));
#9950=CARTESIAN_POINT('',(-0.750555349946514,0.0768195421087394,-9.19165206894919E-17));
#9951=CARTESIAN_POINT('Ctrl Pts',(-0.750555349946514,0.0768195421087394,
-9.19165206894919E-17));
#9952=CARTESIAN_POINT('Ctrl Pts',(-0.562916512459802,-0.0315137912242434,
0.325000000000144));
#9953=CARTESIAN_POINT('Ctrl Pts',(-0.375277674973257,0.0768195421087395,
0.65));
#9954=CARTESIAN_POINT('',(-0.6175,-2.77555756156289E-17,-7.5621939847349E-17));
#9955=CARTESIAN_POINT('',(-0.734027674973257,0.067277284513851,-8.98924642641573E-17));
#9956=CARTESIAN_POINT('Origin',(0.,0.,0.));
#9957=CARTESIAN_POINT('',(-0.375277674973257,0.0768195421087395,-0.65));
#9958=CARTESIAN_POINT('Ctrl Pts',(-0.375277674973257,0.0768195421087395,
-0.65));
#9959=CARTESIAN_POINT('Ctrl Pts',(-0.562916512459968,-0.0315137912242437,
-0.324999999999856));
#9960=CARTESIAN_POINT('Ctrl Pts',(-0.750555349946514,0.0768195421087395,
-9.19165206894919E-17));
#9961=CARTESIAN_POINT('',(0.375277674973257,0.0768195421087395,-0.65));
#9962=CARTESIAN_POINT('Ctrl Pts',(0.375277674973257,0.0768195421087395,
-0.65));
#9963=CARTESIAN_POINT('Ctrl Pts',(-1.66144875635155E-13,-0.0315137912242437,
-0.65));
#9964=CARTESIAN_POINT('Ctrl Pts',(-0.375277674973257,0.0768195421087395,
-0.65));
#9965=CARTESIAN_POINT('',(0.750555349946514,0.0768195421087394,0.));
#9966=CARTESIAN_POINT('Ctrl Pts',(0.750555349946514,0.0768195421087394,
0.));
#9967=CARTESIAN_POINT('Ctrl Pts',(0.562916512459802,-0.0315137912242436,
-0.325000000000144));
#9968=CARTESIAN_POINT('Ctrl Pts',(0.375277674973257,0.0768195421087395,
-0.65));
#9969=CARTESIAN_POINT('Ctrl Pts',(0.375277674973257,0.0768195421087394,
0.65));
#9970=CARTESIAN_POINT('Ctrl Pts',(0.562916512459968,-0.0315137912242439,
0.324999999999856));
#9971=CARTESIAN_POINT('Ctrl Pts',(0.750555349946514,0.0768195421087394,
0.));
#9972=CARTESIAN_POINT('Origin',(0.,0.612722715486149,0.));
#9973=CARTESIAN_POINT('',(-0.6175,0.68,-7.5621939847349E-17));
#9974=CARTESIAN_POINT('Origin',(0.,0.68,0.));
#9975=CARTESIAN_POINT('',(-0.750555349946514,0.603180457891261,-9.19165206894919E-17));
#9976=CARTESIAN_POINT('',(-0.734027674973257,0.612722715486149,-8.98924642641573E-17));
#9977=CARTESIAN_POINT('',(-0.375277674973257,0.603180457891261,0.65));
#9978=CARTESIAN_POINT('Ctrl Pts',(-0.375277674973257,0.603180457891261,
0.65));
#9979=CARTESIAN_POINT('Ctrl Pts',(-0.562916512459968,0.711513791224243,
0.324999999999856));
#9980=CARTESIAN_POINT('Ctrl Pts',(-0.750555349946514,0.603180457891261,
-9.19165206894919E-17));
#9981=CARTESIAN_POINT('',(0.375277674973257,0.603180457891261,0.65));
#9982=CARTESIAN_POINT('Ctrl Pts',(0.375277674973257,0.603180457891261,0.65));
#9983=CARTESIAN_POINT('Ctrl Pts',(-1.66755498298699E-13,0.711513791224244,
0.65));
#9984=CARTESIAN_POINT('Ctrl Pts',(-0.375277674973257,0.603180457891261,
0.65));
#9985=CARTESIAN_POINT('',(0.750555349946514,0.603180457891261,0.));
#9986=CARTESIAN_POINT('Ctrl Pts',(0.750555349946514,0.603180457891261,0.));
#9987=CARTESIAN_POINT('Ctrl Pts',(0.562916512459802,0.711513791224244,0.325000000000144));
#9988=CARTESIAN_POINT('Ctrl Pts',(0.375277674973257,0.603180457891261,0.65));
#9989=CARTESIAN_POINT('',(0.375277674973257,0.603180457891261,-0.65));
#9990=CARTESIAN_POINT('Ctrl Pts',(0.375277674973257,0.603180457891261,-0.65));
#9991=CARTESIAN_POINT('Ctrl Pts',(0.562916512459969,0.711513791224244,-0.324999999999856));
#9992=CARTESIAN_POINT('Ctrl Pts',(0.750555349946514,0.603180457891261,0.));
#9993=CARTESIAN_POINT('',(-0.375277674973257,0.603180457891261,-0.65));
#9994=CARTESIAN_POINT('Ctrl Pts',(-0.375277674973257,0.603180457891261,
-0.65));
#9995=CARTESIAN_POINT('Ctrl Pts',(1.66422431391311E-13,0.711513791224244,
-0.65));
#9996=CARTESIAN_POINT('Ctrl Pts',(0.375277674973257,0.603180457891261,-0.65));
#9997=CARTESIAN_POINT('Ctrl Pts',(-0.750555349946514,0.603180457891261,
-9.19165206894919E-17));
#9998=CARTESIAN_POINT('Ctrl Pts',(-0.562916512459802,0.711513791224244,
-0.325000000000144));
#9999=CARTESIAN_POINT('Ctrl Pts',(-0.375277674973257,0.603180457891261,
-0.65));
#10000=CARTESIAN_POINT('Origin',(0.375277674973257,0.,-0.65));
#10001=CARTESIAN_POINT('',(-0.375277674973257,0.,-0.65));
#10002=CARTESIAN_POINT('',(0.375277674973257,0.,-0.65));
#10003=CARTESIAN_POINT('Origin',(-0.375277674973257,0.,-0.65));
#10004=CARTESIAN_POINT('',(-0.750555349946514,0.,-9.19165206894919E-17));
#10005=CARTESIAN_POINT('Origin',(-0.750555349946514,0.,-9.19165206894919E-17));
#10006=CARTESIAN_POINT('',(-0.375277674973257,0.,0.65));
#10007=CARTESIAN_POINT('Origin',(0.,0.,0.));
#10008=CARTESIAN_POINT('',(-0.338975,0.68,4.15124648740974E-17));
#10009=CARTESIAN_POINT('Origin',(0.,0.68,0.));
#10010=CARTESIAN_POINT('',(-0.338975,0.,4.15124648740974E-17));
#10011=CARTESIAN_POINT('',(-0.338975,0.,4.15124648740974E-17));
#10012=CARTESIAN_POINT('Origin',(0.,0.,0.));
#10013=CARTESIAN_POINT('Origin',(-0.375277674973257,0.,0.65));
#10014=CARTESIAN_POINT('',(0.375277674973257,0.,0.65));
#10015=CARTESIAN_POINT('Origin',(0.750555349946514,0.,0.));
#10016=CARTESIAN_POINT('',(0.750555349946514,0.,0.));
#10017=CARTESIAN_POINT('Origin',(0.375277674973257,0.,0.65));
#10018=CARTESIAN_POINT('Origin',(0.,0.68,-1.11022302462516E-16));
#10019=CARTESIAN_POINT('Origin',(0.,0.,-1.11022302462516E-16));
#10236=UNCERTAINTY_MEASURE_WITH_UNIT(LENGTH_MEASURE(0.001),#10267,
'DISTANCE_ACCURACY_VALUE',
'Maximum model space distance between geometric entities at asserted c
onnectivities');
#10241=UNCERTAINTY_MEASURE_WITH_UNIT(LENGTH_MEASURE(0.001),#10267,
'DISTANCE_ACCURACY_VALUE',
'Maximum model space distance between geometric entities at asserted c
onnectivities');
#10261=(
GEOMETRIC_REPRESENTATION_CONTEXT(3)
GLOBAL_UNCERTAINTY_ASSIGNED_CONTEXT((#10236))
GLOBAL_UNIT_ASSIGNED_CONTEXT((#10267,#10269,#10270))
REPRESENTATION_CONTEXT('','3D')
);
#10266=(
GEOMETRIC_REPRESENTATION_CONTEXT(3)
GLOBAL_UNCERTAINTY_ASSIGNED_CONTEXT((#10241))
GLOBAL_UNIT_ASSIGNED_CONTEXT((#10267,#10269,#10270))
REPRESENTATION_CONTEXT('','3D')
);
#10267=(
LENGTH_UNIT()
NAMED_UNIT(*)
SI_UNIT(.CENTI.,.METRE.)
);
#10269=(
NAMED_UNIT(*)
PLANE_ANGLE_UNIT()
SI_UNIT($,.RADIAN.)
);
#10270=(
NAMED_UNIT(*)
SI_UNIT($,.STERADIAN.)
SOLID_ANGLE_UNIT()
);
#10290=SHAPE_DEFINITION_REPRESENTATION(#10314,#10373);
#10314=PRODUCT_DEFINITION_SHAPE('',$,#10398);
#10373=SHAPE_REPRESENTATION('',(#5448),#10261);
#10378=PRODUCT_DEFINITION_CONTEXT('part definition',#10452,'design');
#10398=PRODUCT_DEFINITION('Hex Nut - M8','Hex Nut - M8',#10422,
#10378);
#10422=PRODUCT_DEFINITION_FORMATION('',$,#10473);
#10452=APPLICATION_CONTEXT(
'Core Data for Automotive Mechanical Design Process');
#10453=PRODUCT_CONTEXT('part definition',#10452,'mechanical');
#10473=PRODUCT('Hex Nut - M8','Hex Nut - M8',
'Hex Nut - M8',(#10453));
#10548=COLOUR_RGB('Black',0.12,0.14,0.17);
#10549=FILL_AREA_STYLE_COLOUR('',#10548);
#10550=FILL_AREA_STYLE('',(#10549));
#10551=SURFACE_STYLE_FILL_AREA(#10550);
#10552=SURFACE_SIDE_STYLE('',(#10551));
#10553=SURFACE_STYLE_USAGE(.BOTH.,#10552);
#10554=PRESENTATION_STYLE_ASSIGNMENT((#10553));
ENDSEC;
END-ISO-10303-21;
